ISO-10303-21;
HEADER;
/* Generated by software containing ST-Developer
 * from STEP Tools, Inc. (www.steptools.com) 
 */

FILE_DESCRIPTION(
/* description */ (''),
/* implementation_level */ '2;1');

FILE_NAME(
/* name */ 'Socket Set Screw - M5x8.step',
/* time_stamp */ '2026-10-29T16:43:51-07:00',
/* author */ (''),
/* organization */ (''),
/* preprocessor_version */ 'ST-DEVELOPER v20.2',
/* originating_system */ 'Autodesk Translation Framework v15.17.0.0',
/* authorisation */ '');

FILE_SCHEMA (('AUTOMOTIVE_DESIGN { 1 0 10303 214 3 1 1 }'));
ENDSEC;

DATA;
#10=MECHANICAL_DESIGN_GEOMETRIC_PRESENTATION_REPRESENTATION('',(#377),#10292);
#305=CONICAL_SURFACE('',#5560,0.235,0.785398163397448);
#306=CONICAL_SURFACE('',#5564,0.2125,0.785398163397448);
#331=SHAPE_REPRESENTATION_RELATIONSHIP('SRR','None',#10427,#354);
#354=ADVANCED_BREP_SHAPE_REPRESENTATION('',(#398),#10279);
#377=STYLED_ITEM('',(#10635),#398);
#398=MANIFOLD_SOLID_BREP('Body1',#5021);
#474=FACE_BOUND('',#1223,.T.);
#625=PLANE('',#5551);
#626=PLANE('',#5552);
#627=PLANE('',#5553);
#628=PLANE('',#5554);
#629=PLANE('',#5555);
#630=PLANE('',#5556);
#631=PLANE('',#5557);
#632=PLANE('',#5558);
#633=PLANE('',#5566);
#859=FACE_OUTER_BOUND('',#1215,.T.);
#860=FACE_OUTER_BOUND('',#1216,.T.);
#861=FACE_OUTER_BOUND('',#1217,.T.);
#862=FACE_OUTER_BOUND('',#1218,.T.);
#863=FACE_OUTER_BOUND('',#1219,.T.);
#864=FACE_OUTER_BOUND('',#1220,.T.);
#865=FACE_OUTER_BOUND('',#1221,.T.);
#866=FACE_OUTER_BOUND('',#1222,.T.);
#867=FACE_OUTER_BOUND('',#1224,.T.);
#868=FACE_OUTER_BOUND('',#1225,.T.);
#869=FACE_OUTER_BOUND('',#1226,.T.);
#870=FACE_OUTER_BOUND('',#1227,.T.);
#1215=EDGE_LOOP('',(#4077,#4078,#4079,#4080));
#1216=EDGE_LOOP('',(#4081,#4082,#4083,#4084));
#1217=EDGE_LOOP('',(#4085,#4086,#4087,#4088));
#1218=EDGE_LOOP('',(#4089,#4090,#4091,#4092));
#1219=EDGE_LOOP('',(#4093,#4094,#4095,#4096));
#1220=EDGE_LOOP('',(#4097,#4098,#4099,#4100));
#1221=EDGE_LOOP('',(#4101,#4102,#4103,#4104,#4105,#4106));
#1222=EDGE_LOOP('',(#4107));
#1223=EDGE_LOOP('',(#4108,#4109,#4110,#4111,#4112,#4113));
#1224=EDGE_LOOP('',(#4114,#4115,#4116,#4117));
#1225=EDGE_LOOP('',(#4118,#4119,#4120,#4121));
#1226=EDGE_LOOP('',(#4122,#4123,#4124,#4125));
#1227=EDGE_LOOP('',(#4126));
#1623=LINE('',#9565,#2015);
#1624=LINE('',#9567,#2016);
#1625=LINE('',#9569,#2017);
#1626=LINE('',#9570,#2018);
#1627=LINE('',#9573,#2019);
#1628=LINE('',#9575,#2020);
#1629=LINE('',#9576,#2021);
#1630=LINE('',#9579,#2022);
#1631=LINE('',#9581,#2023);
#1632=LINE('',#9582,#2024);
#1633=LINE('',#9585,#2025);
#1634=LINE('',#9587,#2026);
#1635=LINE('',#9588,#2027);
#1636=LINE('',#9591,#2028);
#1637=LINE('',#9593,#2029);
#1638=LINE('',#9594,#2030);
#1639=LINE('',#9596,#2031);
#1640=LINE('',#9597,#2032);
#1641=LINE('',#9605,#2033);
#1642=LINE('',#9609,#2034);
#1643=LINE('',#9613,#2035);
#2015=VECTOR('',#6602,1.);
#2016=VECTOR('',#6603,1.);
#2017=VECTOR('',#6604,1.);
#2018=VECTOR('',#6605,1.);
#2019=VECTOR('',#6608,1.);
#2020=VECTOR('',#6609,1.);
#2021=VECTOR('',#6610,1.);
#2022=VECTOR('',#6613,1.);
#2023=VECTOR('',#6614,1.);
#2024=VECTOR('',#6615,1.);
#2025=VECTOR('',#6618,1.);
#2026=VECTOR('',#6619,1.);
#2027=VECTOR('',#6620,1.);
#2028=VECTOR('',#6623,1.);
#2029=VECTOR('',#6624,1.);
#2030=VECTOR('',#6625,1.);
#2031=VECTOR('',#6628,1.);
#2032=VECTOR('',#6629,1.);
#2033=VECTOR('',#6640,0.235);
#2034=VECTOR('',#6645,0.25);
#2035=VECTOR('',#6650,0.2125);
#2294=CIRCLE('',#5559,0.22);
#2295=CIRCLE('',#5561,0.24505);
#2296=CIRCLE('',#5563,0.24505);
#2297=CIRCLE('',#5565,0.175);
#2613=VERTEX_POINT('',#9563);
#2614=VERTEX_POINT('',#9564);
#2615=VERTEX_POINT('',#9566);
#2616=VERTEX_POINT('',#9568);
#2617=VERTEX_POINT('',#9572);
#2618=VERTEX_POINT('',#9574);
#2619=VERTEX_POINT('',#9578);
#2620=VERTEX_POINT('',#9580);
#2621=VERTEX_POINT('',#9584);
#2622=VERTEX_POINT('',#9586);
#2623=VERTEX_POINT('',#9590);
#2624=VERTEX_POINT('',#9592);
#2625=VERTEX_POINT('',#9600);
#2626=VERTEX_POINT('',#9603);
#2627=VERTEX_POINT('',#9607);
#2628=VERTEX_POINT('',#9611);
#3129=EDGE_CURVE('',#2613,#2614,#1623,.T.);
#3130=EDGE_CURVE('',#2613,#2615,#1624,.T.);
#3131=EDGE_CURVE('',#2615,#2616,#1625,.T.);
#3132=EDGE_CURVE('',#2614,#2616,#1626,.T.);
#3133=EDGE_CURVE('',#2617,#2613,#1627,.T.);
#3134=EDGE_CURVE('',#2617,#2618,#1628,.T.);
#3135=EDGE_CURVE('',#2618,#2615,#1629,.T.);
#3136=EDGE_CURVE('',#2619,#2617,#1630,.T.);
#3137=EDGE_CURVE('',#2619,#2620,#1631,.T.);
#3138=EDGE_CURVE('',#2620,#2618,#1632,.T.);
#3139=EDGE_CURVE('',#2621,#2619,#1633,.T.);
#3140=EDGE_CURVE('',#2621,#2622,#1634,.T.);
#3141=EDGE_CURVE('',#2622,#2620,#1635,.T.);
#3142=EDGE_CURVE('',#2623,#2621,#1636,.T.);
#3143=EDGE_CURVE('',#2623,#2624,#1637,.T.);
#3144=EDGE_CURVE('',#2624,#2622,#1638,.T.);
#3145=EDGE_CURVE('',#2614,#2623,#1639,.T.);
#3146=EDGE_CURVE('',#2616,#2624,#1640,.T.);
#3147=EDGE_CURVE('',#2625,#2625,#2294,.T.);
#3148=EDGE_CURVE('',#2626,#2626,#2295,.T.);
#3149=EDGE_CURVE('',#2626,#2625,#1641,.T.);
#3150=EDGE_CURVE('',#2627,#2627,#2296,.F.);
#3151=EDGE_CURVE('',#2627,#2626,#1642,.T.);
#3152=EDGE_CURVE('',#2628,#2628,#2297,.T.);
#3153=EDGE_CURVE('',#2628,#2627,#1643,.T.);
#4077=ORIENTED_EDGE('',*,*,#3129,.F.);
#4078=ORIENTED_EDGE('',*,*,#3130,.T.);
#4079=ORIENTED_EDGE('',*,*,#3131,.T.);
#4080=ORIENTED_EDGE('',*,*,#3132,.F.);
#4081=ORIENTED_EDGE('',*,*,#3133,.F.);
#4082=ORIENTED_EDGE('',*,*,#3134,.T.);
#4083=ORIENTED_EDGE('',*,*,#3135,.T.);
#4084=ORIENTED_EDGE('',*,*,#3130,.F.);
#4085=ORIENTED_EDGE('',*,*,#3136,.F.);
#4086=ORIENTED_EDGE('',*,*,#3137,.T.);
#4087=ORIENTED_EDGE('',*,*,#3138,.T.);
#4088=ORIENTED_EDGE('',*,*,#3134,.F.);
#4089=ORIENTED_EDGE('',*,*,#3139,.F.);
#4090=ORIENTED_EDGE('',*,*,#3140,.T.);
#4091=ORIENTED_EDGE('',*,*,#3141,.T.);
#4092=ORIENTED_EDGE('',*,*,#3137,.F.);
#4093=ORIENTED_EDGE('',*,*,#3142,.F.);
#4094=ORIENTED_EDGE('',*,*,#3143,.T.);
#4095=ORIENTED_EDGE('',*,*,#3144,.T.);
#4096=ORIENTED_EDGE('',*,*,#3140,.F.);
#4097=ORIENTED_EDGE('',*,*,#3145,.F.);
#4098=ORIENTED_EDGE('',*,*,#3132,.T.);
#4099=ORIENTED_EDGE('',*,*,#3146,.T.);
#4100=ORIENTED_EDGE('',*,*,#3143,.F.);
#4101=ORIENTED_EDGE('',*,*,#3146,.F.);
#4102=ORIENTED_EDGE('',*,*,#3131,.F.);
#4103=ORIENTED_EDGE('',*,*,#3135,.F.);
#4104=ORIENTED_EDGE('',*,*,#3138,.F.);
#4105=ORIENTED_EDGE('',*,*,#3141,.F.);
#4106=ORIENTED_EDGE('',*,*,#3144,.F.);
#4107=ORIENTED_EDGE('',*,*,#3147,.F.);
#4108=ORIENTED_EDGE('',*,*,#3129,.T.);
#4109=ORIENTED_EDGE('',*,*,#3145,.T.);
#4110=ORIENTED_EDGE('',*,*,#3142,.T.);
#4111=ORIENTED_EDGE('',*,*,#3139,.T.);
#4112=ORIENTED_EDGE('',*,*,#3136,.T.);
#4113=ORIENTED_EDGE('',*,*,#3133,.T.);
#4114=ORIENTED_EDGE('',*,*,#3148,.F.);
#4115=ORIENTED_EDGE('',*,*,#3149,.T.);
#4116=ORIENTED_EDGE('',*,*,#3147,.T.);
#4117=ORIENTED_EDGE('',*,*,#3149,.F.);
#4118=ORIENTED_EDGE('',*,*,#3150,.F.);
#4119=ORIENTED_EDGE('',*,*,#3151,.T.);
#4120=ORIENTED_EDGE('',*,*,#3148,.T.);
#4121=ORIENTED_EDGE('',*,*,#3151,.F.);
#4122=ORIENTED_EDGE('',*,*,#3152,.F.);
#4123=ORIENTED_EDGE('',*,*,#3153,.T.);
#4124=ORIENTED_EDGE('',*,*,#3150,.T.);
#4125=ORIENTED_EDGE('',*,*,#3153,.F.);
#4126=ORIENTED_EDGE('',*,*,#3152,.T.);
#4679=CYLINDRICAL_SURFACE('',#5562,0.24505);
#4868=ADVANCED_FACE('',(#859),#625,.F.);
#4869=ADVANCED_FACE('',(#860),#626,.F.);
#4870=ADVANCED_FACE('',(#861),#627,.F.);
#4871=ADVANCED_FACE('',(#862),#628,.F.);
#4872=ADVANCED_FACE('',(#863),#629,.F.);
#4873=ADVANCED_FACE('',(#864),#630,.F.);
#4874=ADVANCED_FACE('',(#865),#631,.F.);
#4875=ADVANCED_FACE('',(#866,#474),#632,.T.);
#4876=ADVANCED_FACE('',(#867),#305,.T.);
#4877=ADVANCED_FACE('',(#868),#4679,.T.);
#4878=ADVANCED_FACE('',(#869),#306,.T.);
#4879=ADVANCED_FACE('',(#870),#633,.T.);
#5021=CLOSED_SHELL('',(#4868,#4869,#4870,#4871,#4872,#4873,#4874,#4875,
#4876,#4877,#4878,#4879));
#5550=AXIS2_PLACEMENT_3D('',#9561,#6598,#6599);
#5551=AXIS2_PLACEMENT_3D('',#9562,#6600,#6601);
#5552=AXIS2_PLACEMENT_3D('',#9571,#6606,#6607);
#5553=AXIS2_PLACEMENT_3D('',#9577,#6611,#6612);
#5554=AXIS2_PLACEMENT_3D('',#9583,#6616,#6617);
#5555=AXIS2_PLACEMENT_3D('',#9589,#6621,#6622);
#5556=AXIS2_PLACEMENT_3D('',#9595,#6626,#6627);
#5557=AXIS2_PLACEMENT_3D('',#9598,#6630,#6631);
#5558=AXIS2_PLACEMENT_3D('',#9599,#6632,#6633);
#5559=AXIS2_PLACEMENT_3D('',#9601,#6634,#6635);
#5560=AXIS2_PLACEMENT_3D('',#9602,#6636,#6637);
#5561=AXIS2_PLACEMENT_3D('',#9604,#6638,#6639);
#5562=AXIS2_PLACEMENT_3D('',#9606,#6641,#6642);
#5563=AXIS2_PLACEMENT_3D('',#9608,#6643,#6644);
#5564=AXIS2_PLACEMENT_3D('',#9610,#6646,#6647);
#5565=AXIS2_PLACEMENT_3D('',#9612,#6648,#6649);
#5566=AXIS2_PLACEMENT_3D('',#9614,#6651,#6652);
#6598=DIRECTION('axis',(0.,0.,1.));
#6599=DIRECTION('refdir',(1.,0.,0.));
#6600=DIRECTION('center_axis',(0.866025403784439,0.,-0.5));
#6601=DIRECTION('ref_axis',(0.5,0.,0.866025403784439));
#6602=DIRECTION('',(0.5,0.,0.866025403784439));
#6603=DIRECTION('',(0.,-1.,0.));
#6604=DIRECTION('',(0.5,0.,0.866025403784439));
#6605=DIRECTION('',(0.,-1.,0.));
#6606=DIRECTION('center_axis',(1.92296268638356E-16,0.,-1.));
#6607=DIRECTION('ref_axis',(1.,0.,1.92296268638356E-16));
#6608=DIRECTION('',(1.,0.,1.92296268638356E-16));
#6609=DIRECTION('',(0.,-1.,0.));
#6610=DIRECTION('',(1.,0.,1.92296268638356E-16));
#6611=DIRECTION('center_axis',(-0.866025403784439,0.,-0.5));
#6612=DIRECTION('ref_axis',(0.5,0.,-0.866025403784439));
#6613=DIRECTION('',(0.5,0.,-0.866025403784439));
#6614=DIRECTION('',(0.,-1.,0.));
#6615=DIRECTION('',(0.5,0.,-0.866025403784438));
#6616=DIRECTION('center_axis',(-0.866025403784439,0.,0.5));
#6617=DIRECTION('ref_axis',(-0.5,0.,-0.866025403784439));
#6618=DIRECTION('',(-0.5,0.,-0.866025403784439));
#6619=DIRECTION('',(0.,-1.,0.));
#6620=DIRECTION('',(-0.5,0.,-0.866025403784439));
#6621=DIRECTION('center_axis',(-1.92296268638356E-16,0.,1.));
#6622=DIRECTION('ref_axis',(-1.,0.,-1.92296268638356E-16));
#6623=DIRECTION('',(-1.,0.,-1.92296268638356E-16));
#6624=DIRECTION('',(0.,-1.,0.));
#6625=DIRECTION('',(-1.,0.,-1.92296268638356E-16));
#6626=DIRECTION('center_axis',(0.866025403784439,0.,0.5));
#6627=DIRECTION('ref_axis',(-0.5,0.,0.866025403784439));
#6628=DIRECTION('',(-0.5,0.,0.866025403784439));
#6629=DIRECTION('',(-0.5,0.,0.866025403784439));
#6630=DIRECTION('center_axis',(0.,-1.,0.));
#6631=DIRECTION('ref_axis',(0.,0.,-1.));
#6632=DIRECTION('center_axis',(0.,1.,0.));
#6633=DIRECTION('ref_axis',(0.,0.,1.));
#6634=DIRECTION('center_axis',(0.,-1.,0.));
#6635=DIRECTION('ref_axis',(1.,0.,0.));
#6636=DIRECTION('center_axis',(0.,-1.,0.));
#6637=DIRECTION('ref_axis',(1.,0.,0.));
#6638=DIRECTION('center_axis',(0.,-1.,0.));
#6639=DIRECTION('ref_axis',(1.,0.,0.));
#6640=DIRECTION('',(0.707106781186547,0.707106781186548,8.65956056235493E-17));
#6641=DIRECTION('center_axis',(0.,-1.,0.));
#6642=DIRECTION('ref_axis',(1.,0.,0.));
#6643=DIRECTION('center_axis',(0.,1.,0.));
#6644=DIRECTION('ref_axis',(1.,0.,0.));
#6645=DIRECTION('',(0.,1.,0.));
#6646=DIRECTION('center_axis',(0.,1.,0.));
#6647=DIRECTION('ref_axis',(1.,0.,0.));
#6648=DIRECTION('center_axis',(0.,-1.,0.));
#6649=DIRECTION('ref_axis',(1.,0.,0.));
#6650=DIRECTION('',(-0.707106781186547,0.707106781186548,-8.65956056235493E-17));
#6651=DIRECTION('center_axis',(0.,-1.,0.));
#6652=DIRECTION('ref_axis',(0.,0.,-1.));
#9561=CARTESIAN_POINT('',(0.,0.,0.));
#9562=CARTESIAN_POINT('Origin',(0.0721687836487032,0.,-0.125));
#9563=CARTESIAN_POINT('',(0.0721687836487032,0.,-0.125));
#9564=CARTESIAN_POINT('',(0.144337567297406,0.,0.));
#9565=CARTESIAN_POINT('',(0.117710979560879,0.,-0.0461186027918559));
#9566=CARTESIAN_POINT('',(0.0721687836487032,-0.25,-0.125));
#9567=CARTESIAN_POINT('',(0.0721687836487032,0.,-0.125));
#9568=CARTESIAN_POINT('',(0.144337567297406,-0.25,0.));
#9569=CARTESIAN_POINT('',(0.144337567297406,-0.25,0.));
#9570=CARTESIAN_POINT('',(0.144337567297406,0.,0.));
#9571=CARTESIAN_POINT('Origin',(-0.0721687836487032,0.,-0.125));
#9572=CARTESIAN_POINT('',(-0.0721687836487032,0.,-0.125));
#9573=CARTESIAN_POINT('',(0.0739156081756484,0.,-0.125));
#9574=CARTESIAN_POINT('',(-0.0721687836487032,-0.25,-0.125));
#9575=CARTESIAN_POINT('',(-0.0721687836487032,0.,-0.125));
#9576=CARTESIAN_POINT('',(0.0721687836487032,-0.25,-0.125));
#9577=CARTESIAN_POINT('Origin',(-0.144337567297406,0.,-4.16333634234434E-17));
#9578=CARTESIAN_POINT('',(-0.144337567297406,0.,-1.76762539787485E-17));
#9579=CARTESIAN_POINT('',(-0.0987953713852306,0.,-0.0788813972081442));
#9580=CARTESIAN_POINT('',(-0.144337567297406,-0.25,-2.77555756156289E-17));
#9581=CARTESIAN_POINT('',(-0.144337567297406,0.,-1.76762539787485E-17));
#9582=CARTESIAN_POINT('',(-0.0721687836487032,-0.25,-0.125));
#9583=CARTESIAN_POINT('Origin',(-0.0721687836487033,0.,0.125));
#9584=CARTESIAN_POINT('',(-0.0721687836487033,0.,0.125));
#9585=CARTESIAN_POINT('',(-0.0627109795608791,0.,0.141381397208144));
#9586=CARTESIAN_POINT('',(-0.0721687836487033,-0.25,0.125));
#9587=CARTESIAN_POINT('',(-0.0721687836487033,0.,0.125));
#9588=CARTESIAN_POINT('',(-0.144337567297406,-0.25,-1.76762539787485E-17));
#9589=CARTESIAN_POINT('Origin',(0.0721687836487032,0.,0.125));
#9590=CARTESIAN_POINT('',(0.0721687836487032,0.,0.125));
#9591=CARTESIAN_POINT('',(0.146084391824352,0.,0.125));
#9592=CARTESIAN_POINT('',(0.0721687836487032,-0.25,0.125));
#9593=CARTESIAN_POINT('',(0.0721687836487032,0.,0.125));
#9594=CARTESIAN_POINT('',(-0.0721687836487033,-0.25,0.125));
#9595=CARTESIAN_POINT('Origin',(0.144337567297406,0.,0.));
#9596=CARTESIAN_POINT('',(0.153795371385231,0.,-0.0163813972081441));
#9597=CARTESIAN_POINT('',(0.0721687836487032,-0.25,0.125));
#9598=CARTESIAN_POINT('Origin',(0.,-0.25,0.));
#9599=CARTESIAN_POINT('Origin',(0.22,0.,0.));
#9600=CARTESIAN_POINT('',(-0.22,-8.67361737988404E-18,-2.69422295812418E-17));
#9601=CARTESIAN_POINT('Origin',(0.,0.,0.));
#9602=CARTESIAN_POINT('Origin',(0.,-0.015,0.));
#9603=CARTESIAN_POINT('',(-0.24505,-0.02505,-3.00099698131059E-17));
#9604=CARTESIAN_POINT('Origin',(0.,-0.02505,0.));
#9605=CARTESIAN_POINT('',(-0.235,-0.015,-2.87791997799628E-17));
#9606=CARTESIAN_POINT('Origin',(0.,-0.3775,0.));
#9607=CARTESIAN_POINT('',(-0.24505,-0.72995,3.00099698131059E-17));
#9608=CARTESIAN_POINT('Origin',(0.,-0.72995,0.));
#9609=CARTESIAN_POINT('',(-0.24505,-0.3775,-3.00099698131059E-17));
#9610=CARTESIAN_POINT('Origin',(0.,-0.7625,0.));
#9611=CARTESIAN_POINT('',(-0.175,-0.8,-2.14313189850787E-17));
#9612=CARTESIAN_POINT('Origin',(0.,-0.8,0.));
#9613=CARTESIAN_POINT('',(-0.2125,-0.7625,-2.60237444818813E-17));
#9614=CARTESIAN_POINT('Origin',(0.,-0.8,0.));
#10251=UNCERTAINTY_MEASURE_WITH_UNIT(LENGTH_MEASURE(0.001),#10293,
'DISTANCE_ACCURACY_VALUE',
'Maximum model space distance between geometric entities at asserted c
onnectivities');
#10264=UNCERTAINTY_MEASURE_WITH_UNIT(LENGTH_MEASURE(0.001),#10293,
'DISTANCE_ACCURACY_VALUE',
'Maximum model space distance between geometric entities at asserted c
onnectivities');
#10279=(
GEOMETRIC_REPRESENTATION_CONTEXT(3)
GLOBAL_UNCERTAINTY_ASSIGNED_CONTEXT((#10251))
GLOBAL_UNIT_ASSIGNED_CONTEXT((#10293,#10295,#10296))
REPRESENTATION_CONTEXT('','3D')
);
#10292=(
GEOMETRIC_REPRESENTATION_CONTEXT(3)
GLOBAL_UNCERTAINTY_ASSIGNED_CONTEXT((#10264))
GLOBAL_UNIT_ASSIGNED_CONTEXT((#10293,#10295,#10296))
REPRESENTATION_CONTEXT('','3D')
);
#10293=(
LENGTH_UNIT()
NAMED_UNIT(*)
SI_UNIT(.CENTI.,.METRE.)
);
#10295=(
NAMED_UNIT(*)
PLANE_ANGLE_UNIT()
SI_UNIT($,.RADIAN.)
);
#10296=(
NAMED_UNIT(*)
SI_UNIT($,.STERADIAN.)
SOLID_ANGLE_UNIT()
);
#10311=SHAPE_DEFINITION_REPRESENTATION(#10338,#10427);
#10338=PRODUCT_DEFINITION_SHAPE('',$,#10455);
#10427=SHAPE_REPRESENTATION('',(#5550),#10279);
#10440=PRODUCT_DEFINITION_CONTEXT('part definition',#10523,'design');
#10455=PRODUCT_DEFINITION('Socket Set Screw - M5x8',
'Socket Set Screw - M5x8',#10482,#10440);
#10482=PRODUCT_DEFINITION_FORMATION('',$,#10539);
#10523=APPLICATION_CONTEXT(
'Core Data for Automotive Mechanical Design Process');
#10524=PRODUCT_CONTEXT('part definition',#10523,'mechanical');
#10539=PRODUCT('Socket Set Screw - M5x8','Socket Set Screw - M5x8',
'Socket Set Screw - M5x8',(#10524));
#10629=COLOUR_RGB('Black',0.12,0.14,0.17);
#10630=FILL_AREA_STYLE_COLOUR('',#10629);
#10631=FILL_AREA_STYLE('',(#10630));
#10632=SURFACE_STYLE_FILL_AREA(#10631);
#10633=SURFACE_SIDE_STYLE('',(#10632));
#10634=SURFACE_STYLE_USAGE(.BOTH.,#10633);
#10635=PRESENTATION_STYLE_ASSIGNMENT((#10634));
ENDSEC;
END-ISO-10303-21;
